ISO-10303-21;
HEADER;
/* Generated by software containing ST-Developer
 * from STEP Tools, Inc. (www.steptools.com) 
 */

FILE_DESCRIPTION(
/* description */ ('XY cross-slide table'),
/* implementation_level */ '2;1');

FILE_NAME(
/* name */ 'Socket Set Screw - M5x8.step',
/* time_stamp */ '2026-10-28T03:22:46-07:00',
/* author */ (''),
/* organization */ (''),
/* preprocessor_version */ 'ST-DEVELOPER v20.2',
/* originating_system */ 'Autodesk Translation Framework v15.17.0.0',
/* authorisation */ '');

FILE_SCHEMA (('AUTOMOTIVE_DESIGN { 1 0 10303 214 3 1 1 }'));
ENDSEC;

DATA;
#10=MECHANICAL_DESIGN_GEOMETRIC_PRESENTATION_REPRESENTATION('',(#1724),#62984);
#1461=CONICAL_SURFACE('',#25111,0.235,0.785398163397448);
#1462=CONICAL_SURFACE('',#25115,0.2125,0.785398163397448);
#1543=SHAPE_REPRESENTATION_RELATIONSHIP('SRR','None',#63396,#1626);
#1626=ADVANCED_BREP_SHAPE_REPRESENTATION('',(#1834),#62933);
#1724=STYLED_ITEM('',(#63919),#1834);
#1834=MANIFOLD_SOLID_BREP('Body1',#23021);
#2081=FACE_BOUND('',#4995,.T.);
#2555=PLANE('',#25102);
#2556=PLANE('',#25103);
#2557=PLANE('',#25104);
#2558=PLANE('',#25105);
#2559=PLANE('',#25106);
#2560=PLANE('',#25107);
#2561=PLANE('',#25108);
#2562=PLANE('',#25109);
#2563=PLANE('',#25117);
#3479=FACE_OUTER_BOUND('',#4987,.T.);
#3480=FACE_OUTER_BOUND('',#4988,.T.);
#3481=FACE_OUTER_BOUND('',#4989,.T.);
#3482=FACE_OUTER_BOUND('',#4990,.T.);
#3483=FACE_OUTER_BOUND('',#4991,.T.);
#3484=FACE_OUTER_BOUND('',#4992,.T.);
#3485=FACE_OUTER_BOUND('',#4993,.T.);
#3486=FACE_OUTER_BOUND('',#4994,.T.);
#3487=FACE_OUTER_BOUND('',#4996,.T.);
#3488=FACE_OUTER_BOUND('',#4997,.T.);
#3489=FACE_OUTER_BOUND('',#4998,.T.);
#3490=FACE_OUTER_BOUND('',#4999,.T.);
#4987=EDGE_LOOP('',(#17804,#17805,#17806,#17807));
#4988=EDGE_LOOP('',(#17808,#17809,#17810,#17811));
#4989=EDGE_LOOP('',(#17812,#17813,#17814,#17815));
#4990=EDGE_LOOP('',(#17816,#17817,#17818,#17819));
#4991=EDGE_LOOP('',(#17820,#17821,#17822,#17823));
#4992=EDGE_LOOP('',(#17824,#17825,#17826,#17827));
#4993=EDGE_LOOP('',(#17828,#17829,#17830,#17831,#17832,#17833));
#4994=EDGE_LOOP('',(#17834));
#4995=EDGE_LOOP('',(#17835,#17836,#17837,#17838,#17839,#17840));
#4996=EDGE_LOOP('',(#17841,#17842,#17843,#17844));
#4997=EDGE_LOOP('',(#17845,#17846,#17847,#17848));
#4998=EDGE_LOOP('',(#17849,#17850,#17851,#17852));
#4999=EDGE_LOOP('',(#17853));
#6597=LINE('',#47597,#8084);
#6598=LINE('',#47599,#8085);
#6599=LINE('',#47601,#8086);
#6600=LINE('',#47602,#8087);
#6601=LINE('',#47605,#8088);
#6602=LINE('',#47607,#8089);
#6603=LINE('',#47608,#8090);
#6604=LINE('',#47611,#8091);
#6605=LINE('',#47613,#8092);
#6606=LINE('',#47614,#8093);
#6607=LINE('',#47617,#8094);
#6608=LINE('',#47619,#8095);
#6609=LINE('',#47620,#8096);
#6610=LINE('',#47623,#8097);
#6611=LINE('',#47625,#8098);
#6612=LINE('',#47626,#8099);
#6613=LINE('',#47628,#8100);
#6614=LINE('',#47629,#8101);
#6615=LINE('',#47637,#8102);
#6616=LINE('',#47641,#8103);
#6617=LINE('',#47645,#8104);
#8084=VECTOR('',#29358,1.);
#8085=VECTOR('',#29359,1.);
#8086=VECTOR('',#29360,1.);
#8087=VECTOR('',#29361,1.);
#8088=VECTOR('',#29364,1.);
#8089=VECTOR('',#29365,1.);
#8090=VECTOR('',#29366,1.);
#8091=VECTOR('',#29369,1.);
#8092=VECTOR('',#29370,1.);
#8093=VECTOR('',#29371,1.);
#8094=VECTOR('',#29374,1.);
#8095=VECTOR('',#29375,1.);
#8096=VECTOR('',#29376,1.);
#8097=VECTOR('',#29379,1.);
#8098=VECTOR('',#29380,1.);
#8099=VECTOR('',#29381,1.);
#8100=VECTOR('',#29384,1.);
#8101=VECTOR('',#29385,1.);
#8102=VECTOR('',#29396,0.235);
#8103=VECTOR('',#29401,0.25);
#8104=VECTOR('',#29406,0.2125);
#9295=CIRCLE('',#25110,0.22);
#9296=CIRCLE('',#25112,0.24505);
#9297=CIRCLE('',#25114,0.24505);
#9298=CIRCLE('',#25116,0.175);
#10751=VERTEX_POINT('',#47595);
#10752=VERTEX_POINT('',#47596);
#10753=VERTEX_POINT('',#47598);
#10754=VERTEX_POINT('',#47600);
#10755=VERTEX_POINT('',#47604);
#10756=VERTEX_POINT('',#47606);
#10757=VERTEX_POINT('',#47610);
#10758=VERTEX_POINT('',#47612);
#10759=VERTEX_POINT('',#47616);
#10760=VERTEX_POINT('',#47618);
#10761=VERTEX_POINT('',#47622);
#10762=VERTEX_POINT('',#47624);
#10763=VERTEX_POINT('',#47632);
#10764=VERTEX_POINT('',#47635);
#10765=VERTEX_POINT('',#47639);
#10766=VERTEX_POINT('',#47643);
#13286=EDGE_CURVE('',#10751,#10752,#6597,.T.);
#13287=EDGE_CURVE('',#10751,#10753,#6598,.T.);
#13288=EDGE_CURVE('',#10753,#10754,#6599,.T.);
#13289=EDGE_CURVE('',#10752,#10754,#6600,.T.);
#13290=EDGE_CURVE('',#10755,#10751,#6601,.T.);
#13291=EDGE_CURVE('',#10755,#10756,#6602,.T.);
#13292=EDGE_CURVE('',#10756,#10753,#6603,.T.);
#13293=EDGE_CURVE('',#10757,#10755,#6604,.T.);
#13294=EDGE_CURVE('',#10757,#10758,#6605,.T.);
#13295=EDGE_CURVE('',#10758,#10756,#6606,.T.);
#13296=EDGE_CURVE('',#10759,#10757,#6607,.T.);
#13297=EDGE_CURVE('',#10759,#10760,#6608,.T.);
#13298=EDGE_CURVE('',#10760,#10758,#6609,.T.);
#13299=EDGE_CURVE('',#10761,#10759,#6610,.T.);
#13300=EDGE_CURVE('',#10761,#10762,#6611,.T.);
#13301=EDGE_CURVE('',#10762,#10760,#6612,.T.);
#13302=EDGE_CURVE('',#10752,#10761,#6613,.T.);
#13303=EDGE_CURVE('',#10754,#10762,#6614,.T.);
#13304=EDGE_CURVE('',#10763,#10763,#9295,.T.);
#13305=EDGE_CURVE('',#10764,#10764,#9296,.T.);
#13306=EDGE_CURVE('',#10764,#10763,#6615,.T.);
#13307=EDGE_CURVE('',#10765,#10765,#9297,.F.);
#13308=EDGE_CURVE('',#10765,#10764,#6616,.T.);
#13309=EDGE_CURVE('',#10766,#10766,#9298,.T.);
#13310=EDGE_CURVE('',#10766,#10765,#6617,.T.);
#17804=ORIENTED_EDGE('',*,*,#13286,.F.);
#17805=ORIENTED_EDGE('',*,*,#13287,.T.);
#17806=ORIENTED_EDGE('',*,*,#13288,.T.);
#17807=ORIENTED_EDGE('',*,*,#13289,.F.);
#17808=ORIENTED_EDGE('',*,*,#13290,.F.);
#17809=ORIENTED_EDGE('',*,*,#13291,.T.);
#17810=ORIENTED_EDGE('',*,*,#13292,.T.);
#17811=ORIENTED_EDGE('',*,*,#13287,.F.);
#17812=ORIENTED_EDGE('',*,*,#13293,.F.);
#17813=ORIENTED_EDGE('',*,*,#13294,.T.);
#17814=ORIENTED_EDGE('',*,*,#13295,.T.);
#17815=ORIENTED_EDGE('',*,*,#13291,.F.);
#17816=ORIENTED_EDGE('',*,*,#13296,.F.);
#17817=ORIENTED_EDGE('',*,*,#13297,.T.);
#17818=ORIENTED_EDGE('',*,*,#13298,.T.);
#17819=ORIENTED_EDGE('',*,*,#13294,.F.);
#17820=ORIENTED_EDGE('',*,*,#13299,.F.);
#17821=ORIENTED_EDGE('',*,*,#13300,.T.);
#17822=ORIENTED_EDGE('',*,*,#13301,.T.);
#17823=ORIENTED_EDGE('',*,*,#13297,.F.);
#17824=ORIENTED_EDGE('',*,*,#13302,.F.);
#17825=ORIENTED_EDGE('',*,*,#13289,.T.);
#17826=ORIENTED_EDGE('',*,*,#13303,.T.);
#17827=ORIENTED_EDGE('',*,*,#13300,.F.);
#17828=ORIENTED_EDGE('',*,*,#13303,.F.);
#17829=ORIENTED_EDGE('',*,*,#13288,.F.);
#17830=ORIENTED_EDGE('',*,*,#13292,.F.);
#17831=ORIENTED_EDGE('',*,*,#13295,.F.);
#17832=ORIENTED_EDGE('',*,*,#13298,.F.);
#17833=ORIENTED_EDGE('',*,*,#13301,.F.);
#17834=ORIENTED_EDGE('',*,*,#13304,.F.);
#17835=ORIENTED_EDGE('',*,*,#13286,.T.);
#17836=ORIENTED_EDGE('',*,*,#13302,.T.);
#17837=ORIENTED_EDGE('',*,*,#13299,.T.);
#17838=ORIENTED_EDGE('',*,*,#13296,.T.);
#17839=ORIENTED_EDGE('',*,*,#13293,.T.);
#17840=ORIENTED_EDGE('',*,*,#13290,.T.);
#17841=ORIENTED_EDGE('',*,*,#13305,.F.);
#17842=ORIENTED_EDGE('',*,*,#13306,.T.);
#17843=ORIENTED_EDGE('',*,*,#13304,.T.);
#17844=ORIENTED_EDGE('',*,*,#13306,.F.);
#17845=ORIENTED_EDGE('',*,*,#13307,.F.);
#17846=ORIENTED_EDGE('',*,*,#13308,.T.);
#17847=ORIENTED_EDGE('',*,*,#13305,.T.);
#17848=ORIENTED_EDGE('',*,*,#13308,.F.);
#17849=ORIENTED_EDGE('',*,*,#13309,.F.);
#17850=ORIENTED_EDGE('',*,*,#13310,.T.);
#17851=ORIENTED_EDGE('',*,*,#13307,.T.);
#17852=ORIENTED_EDGE('',*,*,#13310,.F.);
#17853=ORIENTED_EDGE('',*,*,#13309,.T.);
#21333=CYLINDRICAL_SURFACE('',#25113,0.24505);
#22260=ADVANCED_FACE('',(#3479),#2555,.F.);
#22261=ADVANCED_FACE('',(#3480),#2556,.F.);
#22262=ADVANCED_FACE('',(#3481),#2557,.F.);
#22263=ADVANCED_FACE('',(#3482),#2558,.F.);
#22264=ADVANCED_FACE('',(#3483),#2559,.F.);
#22265=ADVANCED_FACE('',(#3484),#2560,.F.);
#22266=ADVANCED_FACE('',(#3485),#2561,.F.);
#22267=ADVANCED_FACE('',(#3486,#2081),#2562,.T.);
#22268=ADVANCED_FACE('',(#3487),#1461,.T.);
#22269=ADVANCED_FACE('',(#3488),#21333,.T.);
#22270=ADVANCED_FACE('',(#3489),#1462,.T.);
#22271=ADVANCED_FACE('',(#3490),#2563,.T.);
#23021=CLOSED_SHELL('',(#22260,#22261,#22262,#22263,#22264,#22265,#22266,
#22267,#22268,#22269,#22270,#22271));
#25101=AXIS2_PLACEMENT_3D('',#47593,#29354,#29355);
#25102=AXIS2_PLACEMENT_3D('',#47594,#29356,#29357);
#25103=AXIS2_PLACEMENT_3D('',#47603,#29362,#29363);
#25104=AXIS2_PLACEMENT_3D('',#47609,#29367,#29368);
#25105=AXIS2_PLACEMENT_3D('',#47615,#29372,#29373);
#25106=AXIS2_PLACEMENT_3D('',#47621,#29377,#29378);
#25107=AXIS2_PLACEMENT_3D('',#47627,#29382,#29383);
#25108=AXIS2_PLACEMENT_3D('',#47630,#29386,#29387);
#25109=AXIS2_PLACEMENT_3D('',#47631,#29388,#29389);
#25110=AXIS2_PLACEMENT_3D('',#47633,#29390,#29391);
#25111=AXIS2_PLACEMENT_3D('',#47634,#29392,#29393);
#25112=AXIS2_PLACEMENT_3D('',#47636,#29394,#29395);
#25113=AXIS2_PLACEMENT_3D('',#47638,#29397,#29398);
#25114=AXIS2_PLACEMENT_3D('',#47640,#29399,#29400);
#25115=AXIS2_PLACEMENT_3D('',#47642,#29402,#29403);
#25116=AXIS2_PLACEMENT_3D('',#47644,#29404,#29405);
#25117=AXIS2_PLACEMENT_3D('',#47646,#29407,#29408);
#29354=DIRECTION('axis',(0.,0.,1.));
#29355=DIRECTION('refdir',(1.,0.,0.));
#29356=DIRECTION('center_axis',(0.866025403784439,0.,-0.5));
#29357=DIRECTION('ref_axis',(0.5,0.,0.866025403784439));
#29358=DIRECTION('',(0.5,0.,0.866025403784439));
#29359=DIRECTION('',(0.,-1.,0.));
#29360=DIRECTION('',(0.5,0.,0.866025403784439));
#29361=DIRECTION('',(0.,-1.,0.));
#29362=DIRECTION('center_axis',(1.92296268638356E-16,0.,-1.));
#29363=DIRECTION('ref_axis',(1.,0.,1.92296268638356E-16));
#29364=DIRECTION('',(1.,0.,1.92296268638356E-16));
#29365=DIRECTION('',(0.,-1.,0.));
#29366=DIRECTION('',(1.,0.,1.92296268638356E-16));
#29367=DIRECTION('center_axis',(-0.866025403784439,0.,-0.5));
#29368=DIRECTION('ref_axis',(0.5,0.,-0.866025403784439));
#29369=DIRECTION('',(0.5,0.,-0.866025403784439));
#29370=DIRECTION('',(0.,-1.,0.));
#29371=DIRECTION('',(0.5,0.,-0.866025403784438));
#29372=DIRECTION('center_axis',(-0.866025403784439,0.,0.5));
#29373=DIRECTION('ref_axis',(-0.5,0.,-0.866025403784439));
#29374=DIRECTION('',(-0.5,0.,-0.866025403784439));
#29375=DIRECTION('',(0.,-1.,0.));
#29376=DIRECTION('',(-0.5,0.,-0.866025403784439));
#29377=DIRECTION('center_axis',(-1.92296268638356E-16,0.,1.));
#29378=DIRECTION('ref_axis',(-1.,0.,-1.92296268638356E-16));
#29379=DIRECTION('',(-1.,0.,-1.92296268638356E-16));
#29380=DIRECTION('',(0.,-1.,0.));
#29381=DIRECTION('',(-1.,0.,-1.92296268638356E-16));
#29382=DIRECTION('center_axis',(0.866025403784439,0.,0.5));
#29383=DIRECTION('ref_axis',(-0.5,0.,0.866025403784439));
#29384=DIRECTION('',(-0.5,0.,0.866025403784439));
#29385=DIRECTION('',(-0.5,0.,0.866025403784439));
#29386=DIRECTION('center_axis',(0.,-1.,0.));
#29387=DIRECTION('ref_axis',(0.,0.,-1.));
#29388=DIRECTION('center_axis',(0.,1.,0.));
#29389=DIRECTION('ref_axis',(0.,0.,1.));
#29390=DIRECTION('center_axis',(0.,-1.,0.));
#29391=DIRECTION('ref_axis',(1.,0.,0.));
#29392=DIRECTION('center_axis',(0.,-1.,0.));
#29393=DIRECTION('ref_axis',(1.,0.,0.));
#29394=DIRECTION('center_axis',(0.,-1.,0.));
#29395=DIRECTION('ref_axis',(1.,0.,0.));
#29396=DIRECTION('',(0.707106781186547,0.707106781186548,8.65956056235493E-17));
#29397=DIRECTION('center_axis',(0.,-1.,0.));
#29398=DIRECTION('ref_axis',(1.,0.,0.));
#29399=DIRECTION('center_axis',(0.,1.,0.));
#29400=DIRECTION('ref_axis',(1.,0.,0.));
#29401=DIRECTION('',(0.,1.,0.));
#29402=DIRECTION('center_axis',(0.,1.,0.));
#29403=DIRECTION('ref_axis',(1.,0.,0.));
#29404=DIRECTION('center_axis',(0.,-1.,0.));
#29405=DIRECTION('ref_axis',(1.,0.,0.));
#29406=DIRECTION('',(-0.707106781186547,0.707106781186548,-8.65956056235493E-17));
#29407=DIRECTION('center_axis',(0.,-1.,0.));
#29408=DIRECTION('ref_axis',(0.,0.,-1.));
#47593=CARTESIAN_POINT('',(0.,0.,0.));
#47594=CARTESIAN_POINT('Origin',(0.0721687836487032,0.,-0.125));
#47595=CARTESIAN_POINT('',(0.0721687836487032,0.,-0.125));
#47596=CARTESIAN_POINT('',(0.144337567297406,0.,0.));
#47597=CARTESIAN_POINT('',(0.117710979560879,0.,-0.0461186027918559));
#47598=CARTESIAN_POINT('',(0.0721687836487032,-0.25,-0.125));
#47599=CARTESIAN_POINT('',(0.0721687836487032,0.,-0.125));
#47600=CARTESIAN_POINT('',(0.144337567297406,-0.25,0.));
#47601=CARTESIAN_POINT('',(0.144337567297406,-0.25,0.));
#47602=CARTESIAN_POINT('',(0.144337567297406,0.,0.));
#47603=CARTESIAN_POINT('Origin',(-0.0721687836487032,0.,-0.125));
#47604=CARTESIAN_POINT('',(-0.0721687836487032,0.,-0.125));
#47605=CARTESIAN_POINT('',(0.0739156081756484,0.,-0.125));
#47606=CARTESIAN_POINT('',(-0.0721687836487032,-0.25,-0.125));
#47607=CARTESIAN_POINT('',(-0.0721687836487032,0.,-0.125));
#47608=CARTESIAN_POINT('',(0.0721687836487032,-0.25,-0.125));
#47609=CARTESIAN_POINT('Origin',(-0.144337567297406,0.,-4.16333634234434E-17));
#47610=CARTESIAN_POINT('',(-0.144337567297406,0.,-1.76762539787485E-17));
#47611=CARTESIAN_POINT('',(-0.0987953713852306,0.,-0.0788813972081442));
#47612=CARTESIAN_POINT('',(-0.144337567297406,-0.25,-2.77555756156289E-17));
#47613=CARTESIAN_POINT('',(-0.144337567297406,0.,-1.76762539787485E-17));
#47614=CARTESIAN_POINT('',(-0.0721687836487032,-0.25,-0.125));
#47615=CARTESIAN_POINT('Origin',(-0.0721687836487033,0.,0.125));
#47616=CARTESIAN_POINT('',(-0.0721687836487033,0.,0.125));
#47617=CARTESIAN_POINT('',(-0.0627109795608791,0.,0.141381397208144));
#47618=CARTESIAN_POINT('',(-0.0721687836487033,-0.25,0.125));
#47619=CARTESIAN_POINT('',(-0.0721687836487033,0.,0.125));
#47620=CARTESIAN_POINT('',(-0.144337567297406,-0.25,-1.76762539787485E-17));
#47621=CARTESIAN_POINT('Origin',(0.0721687836487032,0.,0.125));
#47622=CARTESIAN_POINT('',(0.0721687836487032,0.,0.125));
#47623=CARTESIAN_POINT('',(0.146084391824352,0.,0.125));
#47624=CARTESIAN_POINT('',(0.0721687836487032,-0.25,0.125));
#47625=CARTESIAN_POINT('',(0.0721687836487032,0.,0.125));
#47626=CARTESIAN_POINT('',(-0.0721687836487033,-0.25,0.125));
#47627=CARTESIAN_POINT('Origin',(0.144337567297406,0.,0.));
#47628=CARTESIAN_POINT('',(0.153795371385231,0.,-0.0163813972081441));
#47629=CARTESIAN_POINT('',(0.0721687836487032,-0.25,0.125));
#47630=CARTESIAN_POINT('Origin',(0.,-0.25,0.));
#47631=CARTESIAN_POINT('Origin',(0.22,0.,0.));
#47632=CARTESIAN_POINT('',(-0.22,-8.67361737988404E-18,-2.69422295812418E-17));
#47633=CARTESIAN_POINT('Origin',(0.,0.,0.));
#47634=CARTESIAN_POINT('Origin',(0.,-0.015,0.));
#47635=CARTESIAN_POINT('',(-0.24505,-0.02505,-3.00099698131059E-17));
#47636=CARTESIAN_POINT('Origin',(0.,-0.02505,0.));
#47637=CARTESIAN_POINT('',(-0.235,-0.015,-2.87791997799628E-17));
#47638=CARTESIAN_POINT('Origin',(0.,-0.3775,0.));
#47639=CARTESIAN_POINT('',(-0.24505,-0.72995,3.00099698131059E-17));
#47640=CARTESIAN_POINT('Origin',(0.,-0.72995,0.));
#47641=CARTESIAN_POINT('',(-0.24505,-0.3775,-3.00099698131059E-17));
#47642=CARTESIAN_POINT('Origin',(0.,-0.7625,0.));
#47643=CARTESIAN_POINT('',(-0.175,-0.8,-2.14313189850787E-17));
#47644=CARTESIAN_POINT('Origin',(0.,-0.8,0.));
#47645=CARTESIAN_POINT('',(-0.2125,-0.7625,-2.60237444818813E-17));
#47646=CARTESIAN_POINT('Origin',(0.,-0.8,0.));
#62834=UNCERTAINTY_MEASURE_WITH_UNIT(LENGTH_MEASURE(0.001),#62985,
'DISTANCE_ACCURACY_VALUE',
'Maximum model space distance between geometric entities at asserted c
onnectivities');
#62885=UNCERTAINTY_MEASURE_WITH_UNIT(LENGTH_MEASURE(0.001),#62985,
'DISTANCE_ACCURACY_VALUE',
'Maximum model space distance between geometric entities at asserted c
onnectivities');
#62933=(
GEOMETRIC_REPRESENTATION_CONTEXT(3)
GLOBAL_UNCERTAINTY_ASSIGNED_CONTEXT((#62834))
GLOBAL_UNIT_ASSIGNED_CONTEXT((#62985,#62987,#62988))
REPRESENTATION_CONTEXT('','3D')
);
#62984=(
GEOMETRIC_REPRESENTATION_CONTEXT(3)
GLOBAL_UNCERTAINTY_ASSIGNED_CONTEXT((#62885))
GLOBAL_UNIT_ASSIGNED_CONTEXT((#62985,#62987,#62988))
REPRESENTATION_CONTEXT('','3D')
);
#62985=(
LENGTH_UNIT()
NAMED_UNIT(*)
SI_UNIT(.CENTI.,.METRE.)
);
#62987=(
NAMED_UNIT(*)
PLANE_ANGLE_UNIT()
SI_UNIT($,.RADIAN.)
);
#62988=(
NAMED_UNIT(*)
SI_UNIT($,.STERADIAN.)
SOLID_ANGLE_UNIT()
);
#63036=SHAPE_DEFINITION_REPRESENTATION(#63167,#63396);
#63167=PRODUCT_DEFINITION_SHAPE('',$,#63495);
#63396=SHAPE_REPRESENTATION('',(#25101),#62933);
#63447=PRODUCT_DEFINITION_CONTEXT('part definition',#63743,'design');
#63495=PRODUCT_DEFINITION('Socket Set Screw - M5x8',
'Socket Set Screw - M5x8',#63593,#63447);
#63593=PRODUCT_DEFINITION_FORMATION('',$,#63792);
#63743=APPLICATION_CONTEXT(
'Core Data for Automotive Mechanical Design Process');
#63744=PRODUCT_CONTEXT('part definition',#63743,'mechanical');
#63792=PRODUCT('Socket Set Screw - M5x8','Socket Set Screw - M5x8',
'Socket Set Screw - M5x8',(#63744));
#63913=COLOUR_RGB('Black',0.12,0.14,0.17);
#63914=FILL_AREA_STYLE_COLOUR('',#63913);
#63915=FILL_AREA_STYLE('',(#63914));
#63916=SURFACE_STYLE_FILL_AREA(#63915);
#63917=SURFACE_SIDE_STYLE('',(#63916));
#63918=SURFACE_STYLE_USAGE(.BOTH.,#63917);
#63919=PRESENTATION_STYLE_ASSIGNMENT((#63918));
ENDSEC;
END-ISO-10303-21;
